ISO-10303-21;
HEADER;
/* Generated by software containing ST-Developer
 * from STEP Tools, Inc. (www.steptools.com) 
 */
/* OPTION: using custom renumber hook */

FILE_DESCRIPTION(
/* description */ ('STEP AP242 Edition 2', 'CAx-IF Rec.Pracs.---Representation and Presentation of Product Manufa
cturing Information (PMI)---4.0---2014-10-13', 'CAx-IF Rec.Pracs.---3D Tessellated Geometry---0.4---2014-09-14', '2;1', 'CAx-IF Rec.Pracs.---User Defined Attributes---1.5---2016-08-15'),
/* implementation_level */ '2;1');

FILE_NAME(
/* name */ 'ball.step',
/* time_stamp */ '2026-10-08T12:15:07Z',
/* author */ (''),
/* organization */ (''),
/* preprocessor_version */ 'ST-DEVELOPER v20',
/* originating_system */ 'ONSHAPE BY PTC INC, 1.221',
/* authorisation */ '  ');

FILE_SCHEMA (('AP242_MANAGED_MODEL_BASED_3D_ENGINEERING_MIM_LF { 1 0 10303 442 3 1 4 }'));
ENDSEC;

DATA;
#13=VERTEX_LOOP('',#8257);
#17=SPHERICAL_SURFACE('',#14761,0.0025);
#60=COLOUR_RGB('', 0.66274510, 0.83137255, 0.94901961);
#218=SHAPE_REPRESENTATION_RELATIONSHIP('','',#13792,#245);
#245=ADVANCED_BREP_SHAPE_REPRESENTATION('',(#13736),#45482);
#8257=VERTEX_POINT('',#35181);
#12268=FACE_BOUND('',#13,.T.);
#13212=ADVANCED_FACE('',(#12268),#17,.T.);
#13519=CLOSED_SHELL('',(#13212));
#13546=STYLED_ITEM('',(#13573),#13736);
#13573=PRESENTATION_STYLE_ASSIGNMENT((#13600));
#13600=SURFACE_STYLE_USAGE(.BOTH.,#13627);
#13627=SURFACE_SIDE_STYLE('',(#13654));
#13654=SURFACE_STYLE_FILL_AREA(#13681);
#13681=FILL_AREA_STYLE('',(#13708));
#13708=FILL_AREA_STYLE_COLOUR('',#60);
#13736=MANIFOLD_SOLID_BREP('ball',#13519);
#13764=SHAPE_DEFINITION_REPRESENTATION(#45561,#13792);
#13792=SHAPE_REPRESENTATION('ball',(#13802),#45482);
#13802=AXIS2_PLACEMENT_3D('',#19109,#15295,#15296);
#14761=AXIS2_PLACEMENT_3D('',#35180,#17719,#17720);
#15295=DIRECTION('',(0.,0.,1.));
#15296=DIRECTION('',(1.,0.,0.));
#17719=DIRECTION('',(0.,-1.,0.));
#17720=DIRECTION('',(-1.,0.,0.));
#19109=CARTESIAN_POINT('',(0.,0.,0.));
#35180=CARTESIAN_POINT('',(0.,0.,-0.0245189377942895));
#35181=CARTESIAN_POINT('',(-1.53080849893419E-19,0.0025,-0.0245189377942895));
#45463=MECHANICAL_DESIGN_GEOMETRIC_PRESENTATION_REPRESENTATION('',(#13546),#45464);
#45464=(
GEOMETRIC_REPRESENTATION_CONTEXT(3)
GLOBAL_UNCERTAINTY_ASSIGNED_CONTEXT((#45492))
GLOBAL_UNIT_ASSIGNED_CONTEXT((#45522,#45521,#45520))
REPRESENTATION_CONTEXT('MAS-690','TOP_LEVEL_ASSEMBLY_PART')
);
#45482=(
GEOMETRIC_REPRESENTATION_CONTEXT(3)
GLOBAL_UNCERTAINTY_ASSIGNED_CONTEXT((#45510))
GLOBAL_UNIT_ASSIGNED_CONTEXT((#45522,#45521,#45520))
REPRESENTATION_CONTEXT('ball','COMPONENT_PART')
);
#45492=UNCERTAINTY_MEASURE_WITH_UNIT(LENGTH_MEASURE(1.E-8),#45522,
'DISTANCE_ACCURACY_VALUE','Maximum Tolerance applied to model');
#45510=UNCERTAINTY_MEASURE_WITH_UNIT(LENGTH_MEASURE(1.E-8),#45522,
'DISTANCE_ACCURACY_VALUE','Maximum Tolerance applied to model');
#45520=(
NAMED_UNIT(*)
SI_UNIT($,.STERADIAN.)
SOLID_ANGLE_UNIT()
);
#45521=(
NAMED_UNIT(*)
PLANE_ANGLE_UNIT()
SI_UNIT($,.RADIAN.)
);
#45522=(
LENGTH_UNIT()
NAMED_UNIT(*)
SI_UNIT($,.METRE.)
);
#45561=PRODUCT_DEFINITION_SHAPE('','',#45603);
#45603=PRODUCT_DEFINITION('','',#45659,#45631);
#45631=PRODUCT_DEFINITION_CONTEXT('',#45782,'design');
#45659=PRODUCT_DEFINITION_FORMATION_WITH_SPECIFIED_SOURCE('','',#45715,
 .NOT_KNOWN.);
#45715=PRODUCT('ball','ball','ball',(#45771));
#45771=PRODUCT_CONTEXT('',#45782,'mechanical');
#45782=APPLICATION_CONTEXT('managed model based 3d engineering');
ENDSEC;
END-ISO-10303-21;
